ISO-10303-21;
HEADER;
FILE_DESCRIPTION (('STEP AP214'),
    '1' );
FILE_NAME ('13. Bolt M6x45.step',
    '2026-10-09T08:13:37',
    ( '' ),
    ( '' ),
    'SwSTEP 2.0',
    'SolidWorks 2021',
    '' );
FILE_SCHEMA (( 'AUTOMOTIVE_DESIGN' ));
ENDSEC;

DATA;
#85=CIRCLE ( 'NONE', #4622, 3.000000000000000444 ) ;
#145=AXIS2_PLACEMENT_3D ( 'NONE', #37722, #53827, #52228 ) ;
#174=VECTOR ( 'NONE', #68890, 1000.000000000000114 ) ;
#214=CARTESIAN_POINT ( 'NONE',  ( 8.082903768654762899, -1.269775441351268174E-15, 1.082903768654759125 ) ) ;
#285=DIRECTION ( 'NONE',  ( -0.000000000000000000, -1.000000000000000000, -0.000000000000000000 ) ) ;
#363=( NAMED_UNIT ( * ) PLANE_ANGLE_UNIT ( ) SI_UNIT ( $, .RADIAN. ) );
#583=VERTEX_POINT ( 'NONE', #9173 ) ;
#626=CARTESIAN_POINT ( 'NONE',  ( 3.000000000000000444, 3.673940397442059868E-16, 7.500000000000000000 ) ) ;
#632=ORIENTED_EDGE ( 'NONE', *, *, #3874, .T. ) ;
#829=EDGE_CURVE ( 'NONE', #11857, #12490, #26513, .T. ) ;
#1075=CIRCLE ( 'NONE', #56169, 4.750000000000000000 ) ;
#1159=CARTESIAN_POINT ( 'NONE',  ( -5.000000000000000000, 0.000000000000000000, 0.2499999999999941436 ) ) ;
#1257=CARTESIAN_POINT ( 'NONE',  ( 6.418790567836331284, -2.882328613363594361, 0.02778322089669375133 ) ) ;
#1267=TOROIDAL_SURFACE ( 'NONE', #6956, 4.750000000000000000, 0.2500000000000000000 ) ;
#1380=AXIS2_PLACEMENT_3D ( 'NONE', #55149, #60428, #12235 ) ;
#1409=( NAMED_UNIT ( * ) SI_UNIT ( $, .STERADIAN. ) SOLID_ANGLE_UNIT ( ) );
#1573=DIRECTION ( 'NONE',  ( 0.000000000000000000, 0.000000000000000000, 1.000000000000000000 ) ) ;
#1581=DIRECTION ( 'NONE',  ( -1.000000000000000000, 0.000000000000000000, -0.000000000000000000 ) ) ;
#1670=CARTESIAN_POINT ( 'NONE',  ( 4.041451884327379673, -7.000000000000002665, 7.500000000000000000 ) ) ;
#1715=ADVANCED_FACE ( 'NONE', ( #22942 ), #38109, .F. ) ;
#1767=ORIENTED_EDGE ( 'NONE', *, *, #3874, .F. ) ;
#1914=B_SPLINE_CURVE_WITH_KNOTS ( 'NONE', 3,
 ( #36287, #52107, #26018, #25672, #3859, #53132, #47552, #25341 ),
 .UNSPECIFIED., .F., .F.,
 ( 4, 2, 2, 4 ),
 ( 2.544316211732959925E-07, 0.002094919859796807744, 0.003142252573884623743, 0.004189585287972440175 ),
 .UNSPECIFIED. ) ;
#1963=ORIENTED_EDGE ( 'NONE', *, *, #43566, .F. ) ;
#2004=CYLINDRICAL_SURFACE ( 'NONE', #18014, 5.000000000000000000 ) ;
#2021=VECTOR ( 'NONE', #11905, 1000.000000000000000 ) ;
#2024=AXIS2_PLACEMENT_3D ( 'NONE', #3398, #36883, #47459 ) ;
#2081=ORIENTED_EDGE ( 'NONE', *, *, #41810, .T. ) ;
#2171=FACE_OUTER_BOUND ( 'NONE', #43803, .T. ) ;
#2180=EDGE_LOOP ( 'NONE', ( #39281, #38695, #64548, #13878, #24453 ) ) ;
#2196=( GEOMETRIC_REPRESENTATION_CONTEXT ( 3 ) GLOBAL_UNCERTAINTY_ASSIGNED_CONTEXT ( ( #57207 ) ) GLOBAL_UNIT_ASSIGNED_CONTEXT ( ( #30997, #57749, #47943 ) ) REPRESENTATION_CONTEXT ( 'NONE', 'WORKASPACE' ) );
#2304=CARTESIAN_POINT ( 'NONE',  ( 5.710692600061826774, -4.108790270285303414, 4.269046054161672230E-16 ) ) ;
#2485=ADVANCED_FACE ( 'NONE', ( #41619 ), #63035, .T. ) ;
#2491=AXIS2_PLACEMENT_3D ( 'NONE', #9952, #52871, #4650 ) ;
#2516=EDGE_CURVE ( 'NONE', #22068, #8806, #51985, .T. ) ;
#2556=AXIS2_PLACEMENT_3D ( 'NONE', #29166, #8451, #51348 ) ;
#2623=CARTESIAN_POINT ( 'NONE',  ( -7.440601873764707719, -1.112499515747335854, 0.4948905776603325646 ) ) ;
#2943=( LENGTH_UNIT ( ) NAMED_UNIT ( * ) SI_UNIT ( .MILLI., .METRE. ) );
#3060=FACE_OUTER_BOUND ( 'NONE', #24221, .T. ) ;
#3083=FACE_OUTER_BOUND ( 'NONE', #41325, .T. ) ;
#3259=DIRECTION ( 'NONE',  ( 1.000000000000000000, 0.000000000000000000, 0.000000000000000000 ) ) ;
#3380=B_SPLINE_CURVE_WITH_KNOTS ( 'NONE', 3,
 ( #32732, #22533, #54183, #5996, #63705, #53174, #15549, #65074 ),
 .UNSPECIFIED., .F., .F.,
 ( 4, 2, 2, 4 ),
 ( 0.007148677244982143929, 0.009235234034391179292, 0.01027851242909569654, 0.01132179082380021552 ),
 .UNSPECIFIED. ) ;
#3397=DIRECTION ( 'NONE',  ( 0.000000000000000000, 0.000000000000000000, -1.000000000000000000 ) ) ;
#3398=CARTESIAN_POINT ( 'NONE',  ( 0.000000000000000000, 0.000000000000000000, 0.000000000000000000 ) ) ;
#3590=MANIFOLD_SOLID_BREP ( 'Fillet1', #8176 ) ;
#3613=CARTESIAN_POINT ( 'NONE',  ( 0.000000000000000000, 0.000000000000000000, 7.500000000000000000 ) ) ;
#3662=ORIENTED_EDGE ( 'NONE', *, *, #67500, .F. ) ;
#3768=FACE_OUTER_BOUND ( 'NONE', #35734, .T. ) ;
#3831=EDGE_LOOP ( 'NONE', ( #59555, #27502, #52542, #51282, #28508, #11196 ) ) ;
#3845=DIRECTION ( 'NONE',  ( -1.000000000000000000, 0.000000000000000000, 0.000000000000000000 ) ) ;
#3853=CARTESIAN_POINT ( 'NONE',  ( -7.441974819423180065, 1.110121504110840762, 0.4967607073414712637 ) ) ;
#3859=CARTESIAN_POINT ( 'NONE',  ( -5.356721384544678166, -4.721886399977921478, 0.1324414877861183337 ) ) ;
#3874=EDGE_CURVE ( 'NONE', #583, #49555, #43545, .T. ) ;
#4048=EDGE_CURVE ( 'NONE', #22068, #24120, #59316, .T. ) ;
#4111=CARTESIAN_POINT ( 'NONE',  ( 0.000000000000000000, 0.000000000000000000, 0.2499999999999941436 ) ) ;
#4121=PRESENTATION_STYLE_ASSIGNMENT (( #24901 ) ) ;
#4189=CIRCLE ( 'NONE', #35669, 7.000000000000001776 ) ;
#4368=B_SPLINE_CURVE_WITH_KNOTS ( 'NONE', 3,
 ( #32388, #26756, #63385, #27102, #52510, #37748, #9600, #5310 ),
 .UNSPECIFIED., .F., .F.,
 ( 4, 2, 2, 4 ),
 ( 2.544316211733585141E-07, 0.002094919859796809478, 0.003142252573884625911, 0.004189585287972442777 ),
 .UNSPECIFIED. ) ;
#4430=CARTESIAN_POINT ( 'NONE',  ( 2.418535808707046542, -7.000000000000002665, 0.3989014552058374741 ) ) ;
#4622=AXIS2_PLACEMENT_3D ( 'NONE', #21106, #11588, #32007 ) ;
#4650=DIRECTION ( 'NONE',  ( -1.000000000000000000, 0.000000000000000000, 0.000000000000000000 ) ) ;
#4986=CARTESIAN_POINT ( 'NONE',  ( 0.000000000000000000, -7.000000000000000888, 0.000000000000000000 ) ) ;
#4988=CARTESIAN_POINT ( 'NONE',  ( -4.357963766315036125, 6.451785339198147007, 0.7663918866669852115 ) ) ;
#5141=CARTESIAN_POINT ( 'NONE',  ( 3.728548500389071485, -7.000000000000003553, 0.9264520766856032541 ) ) ;
#5164=CARTESIAN_POINT ( 'NONE',  ( 0.000000000000000000, 0.000000000000000000, 0.000000000000000000 ) ) ;
#5207=EDGE_LOOP ( 'NONE', ( #56502, #67294, #36694, #3662 ) ) ;
#5310=CARTESIAN_POINT ( 'NONE',  ( 6.062177826491070398, 3.500000000000002665, 0.000000000000000000 ) ) ;
#5827=CARTESIAN_POINT ( 'NONE',  ( 2.755511676787088415, -7.000000000000004441, 0.5168645644872222888 ) ) ;
#5885=DIRECTION ( 'NONE',  ( -0.000000000000000000, -0.000000000000000000, -1.000000000000000000 ) ) ;
#5996=CARTESIAN_POINT ( 'NONE',  ( -1.744870598150812802, 7.000000000000005329, 0.2069669095365387901 ) ) ;
#6234=ORIENTED_EDGE ( 'NONE', *, *, #2516, .F. ) ;
#6325=CARTESIAN_POINT ( 'NONE',  ( 0.000000000000000000, 0.000000000000000000, 1.000000000000000000 ) ) ;
#6333=CARTESIAN_POINT ( 'NONE',  ( 8.082903768654762899, -1.269775441351268174E-15, 1.082903768654759125 ) ) ;
#6411=PRODUCT_DEFINITION ( 'UNKNOWN', '', #18035, #56437 ) ;
#6498=PRODUCT_CONTEXT ( 'NONE', #13175, 'mechanical' ) ;
#6501=CARTESIAN_POINT ( 'NONE',  ( 4.750000000000000000, 5.970153145843347347E-16, 1.000000000000000000 ) ) ;
#6592=CARTESIAN_POINT ( 'NONE',  ( -6.062177826491071286, 3.500000000000000888, 0.000000000000000000 ) ) ;
#6600=ORIENTED_EDGE ( 'NONE', *, *, #2516, .T. ) ;
#6694=AXIS2_PLACEMENT_3D ( 'NONE', #66267, #39233, #56409 ) ;
#6956=AXIS2_PLACEMENT_3D ( 'NONE', #13903, #51198, #39623 ) ;
#7113=CARTESIAN_POINT ( 'NONE',  ( 1.401671290772265266, 7.000000000000007105, 0.1093172352041303641 ) ) ;
#7211=LINE ( 'NONE', #34973, #8922 ) ;
#7217=DIRECTION ( 'NONE',  ( 0.000000000000000000, 0.000000000000000000, 1.000000000000000000 ) ) ;
#7347=DIRECTION ( 'NONE',  ( 1.000000000000000000, 0.000000000000000000, 0.000000000000000000 ) ) ;
#7494=B_SPLINE_CURVE_WITH_KNOTS ( 'NONE', 3,
 ( #12222, #2304, #40054, #18572, #44648, #23479 ),
 .UNSPECIFIED., .F., .F.,
 ( 4, 2, 4 ),
 ( 0.004189585287972439308, 0.006269578072783813308, 0.008349570857595188175 ),
 .UNSPECIFIED. ) ;
#7598=ORIENTED_EDGE ( 'NONE', *, *, #29025, .T. ) ;
#7662=ORIENTED_EDGE ( 'NONE', *, *, #64592, .F. ) ;
#7864=CARTESIAN_POINT ( 'NONE',  ( 0.000000000000000000, 0.000000000000000000, 52.50000000000000000 ) ) ;
#7900=CARTESIAN_POINT ( 'NONE',  ( -2.755190520427473366, -7.000000000000002665, 0.4949495880430740402 ) ) ;
#7945=CARTESIAN_POINT ( 'NONE',  ( -6.062177826491072175, -3.499999999999998668, 0.000000000000000000 ) ) ;
#7949=VERTEX_POINT ( 'NONE', #16476 ) ;
#8176=CLOSED_SHELL ( 'NONE', ( #59305, #46605, #11355, #35910, #16438, #1715, #62884, #23066, #42851, #41720, #23044, #35090, #2485, #37379, #19521, #33490, #55726, #27197, #59492, #13173, #61829, #40855, #64943, #17949, #22466 ) ) ;
#8229=VERTEX_POINT ( 'NONE', #29845 ) ;
#8268=CARTESIAN_POINT ( 'NONE',  ( -1.403516486455608892, -7.000000000000002665, 0.1310752030855618366 ) ) ;
#8312=CARTESIAN_POINT ( 'NONE',  ( -6.759171781091402487, -2.292771058063873379, 0.1074872947962660502 ) ) ;
#8407=( LENGTH_UNIT ( ) NAMED_UNIT ( * ) SI_UNIT ( .MILLI., .METRE. ) );
#8451=DIRECTION ( 'NONE',  ( 0.000000000000000000, 0.000000000000000000, -1.000000000000000000 ) ) ;
#8739=FILL_AREA_STYLE_COLOUR ( '', #39367 ) ;
#8806=VERTEX_POINT ( 'NONE', #57029 ) ;
#8922=VECTOR ( 'NONE', #61000, 1000.000000000000000 ) ;
#8943=FACE_OUTER_BOUND ( 'NONE', #35083, .T. ) ;
#8952=CARTESIAN_POINT ( 'NONE',  ( 6.413663052920311358, 2.891209729714700138, -4.192813088908785199E-16 ) ) ;
#8983=AXIS2_PLACEMENT_3D ( 'NONE', #34805, #67517, #56259 ) ;
#9173=CARTESIAN_POINT ( 'NONE',  ( -5.249999999999991118, 0.000000000000000000, 0.000000000000000000 ) ) ;
#9179=CARTESIAN_POINT ( 'NONE',  ( -6.239160159721279797, 3.193457606803199678, 3.307663659028042824E-15 ) ) ;
#9600=CARTESIAN_POINT ( 'NONE',  ( 5.885195493260862776, 3.806542393196805651, -4.285986713106759716E-16 ) ) ;
#9607=DIRECTION ( 'NONE',  ( -1.000000000000000000, 0.000000000000000000, 0.000000000000000000 ) ) ;
#9733=EDGE_CURVE ( 'NONE', #17965, #32986, #4368, .T. ) ;
#9933=ORIENTED_EDGE ( 'NONE', *, *, #31239, .T. ) ;
#9952=CARTESIAN_POINT ( 'NONE',  ( 0.000000000000000000, 0.000000000000000000, 0.000000000000000000 ) ) ;
#10139=VERTEX_POINT ( 'NONE', #14406 ) ;
#10271=CARTESIAN_POINT ( 'NONE',  ( 0.000000000000000000, 0.000000000000000000, 0.000000000000000000 ) ) ;
#10289=EDGE_CURVE ( 'NONE', #53965, #25042, #27708, .T. ) ;
#10318=CIRCLE ( 'NONE', #54117, 7.000000000000001776 ) ;
#10470=DIRECTION ( 'NONE',  ( 1.000000000000000000, 0.000000000000000000, 0.000000000000000000 ) ) ;
#10979=( LENGTH_UNIT ( ) NAMED_UNIT ( * ) SI_UNIT ( .MILLI., .METRE. ) );
#11101=ORIENTED_EDGE ( 'NONE', *, *, #55186, .T. ) ;
#11146=DIRECTION ( 'NONE',  ( -0.8660254037844384856, 0.5000000000000003331, 0.000000000000000000 ) ) ;
#11196=ORIENTED_EDGE ( 'NONE', *, *, #49273, .T. ) ;
#11234=DIRECTION ( 'NONE',  ( 0.000000000000000000, 0.000000000000000000, 1.000000000000000000 ) ) ;
#11355=ADVANCED_FACE ( 'NONE', ( #3060 ), #2004, .F. ) ;
#11418=CONICAL_SURFACE ( 'NONE', #145, 7.000000000000000888, 0.7853981633974500554 ) ;
#11476=MECHANICAL_DESIGN_GEOMETRIC_PRESENTATION_REPRESENTATION('',(#56418),#31671);
#11498=PLANE ( 'NONE',  #39822 ) ;
#11588=DIRECTION ( 'NONE',  ( 0.000000000000000000, 0.000000000000000000, 1.000000000000000000 ) ) ;
#11725=ORIENTED_EDGE ( 'NONE', *, *, #65183, .T. ) ;
#11857=VERTEX_POINT ( 'NONE', #22953 ) ;
#11903=EDGE_CURVE ( 'NONE', #52357, #17965, #60440, .T. ) ;
#11905=DIRECTION ( 'NONE',  ( -0.000000000000000000, -0.000000000000000000, -1.000000000000000000 ) ) ;
#12024=CARTESIAN_POINT ( 'NONE',  ( -4.041451884327381450, -7.000000000000002665, 7.500000000000000000 ) ) ;
#12161=EDGE_LOOP ( 'NONE', ( #27544, #55232, #60223 ) ) ;
#12204=VECTOR ( 'NONE', #5885, 1000.000000000000000 ) ;
#12222=CARTESIAN_POINT ( 'NONE',  ( 6.062177826491071286, -3.500000000000002220, 0.000000000000000000 ) ) ;
#12235=DIRECTION ( 'NONE',  ( -0.4999999999999997780, 0.8660254037844387076, 0.000000000000000000 ) ) ;
#12300=VERTEX_POINT ( 'NONE', #18277 ) ;
#12432=ORIENTED_EDGE ( 'NONE', *, *, #31834, .F. ) ;
#12439=PLANE ( 'NONE',  #61129 ) ;
#12448=FACE_OUTER_BOUND ( 'NONE', #2180, .T. ) ;
#12454=EDGE_CURVE ( 'NONE', #27631, #10139, #59025, .T. ) ;
#12490=VERTEX_POINT ( 'NONE', #31227 ) ;
#12506=CARTESIAN_POINT ( 'NONE',  ( 0.000000000000000000, 0.000000000000000000, 0.000000000000000000 ) ) ;
#12662=CONICAL_SURFACE ( 'NONE', #38591, 5.000000000000000000, 0.7853981633974415066 ) ;
#12689=CIRCLE ( 'NONE', #2556, 5.000000000000000000 ) ;
#12805=PLANE ( 'NONE',  #6694 ) ;
#12812=CARTESIAN_POINT ( 'NONE',  ( 0.000000000000000000, 0.000000000000000000, 0.000000000000000000 ) ) ;
#13140=DIRECTION ( 'NONE',  ( 1.000000000000000000, 0.000000000000000000, -0.000000000000000000 ) ) ;
#13164=EDGE_CURVE ( 'NONE', #17330, #21751, #14221, .T. ) ;
#13173=ADVANCED_FACE ( 'NONE', ( #8943 ), #11418, .T. ) ;
#13175=APPLICATION_CONTEXT ( 'automotive_design' ) ;
#13192=AXIS2_PLACEMENT_3D ( 'NONE', #63679, #285, #21815 ) ;
#13265=PLANE ( 'NONE',  #67808 ) ;
#13275=CARTESIAN_POINT ( 'NONE',  ( 8.082903768654762899, -1.105959442090949618E-15, 7.500000000000000000 ) ) ;
#13312=DIRECTION ( 'NONE',  ( -1.000000000000000000, 0.000000000000000000, 0.000000000000000000 ) ) ;
#13463=ORIENTED_EDGE ( 'NONE', *, *, #36212, .F. ) ;
#13539=FILL_AREA_STYLE_COLOUR ( '', #67625 ) ;
#13634=AXIS2_PLACEMENT_3D ( 'NONE', #43859, #49131, #66304 ) ;
#13877=CARTESIAN_POINT ( 'NONE',  ( 6.759171781091401598, 2.292771058063876932, 0.1074872947962648290 ) ) ;
#13878=ORIENTED_EDGE ( 'NONE', *, *, #43814, .T. ) ;
#13903=CARTESIAN_POINT ( 'NONE',  ( 0.000000000000000000, 0.000000000000000000, 0.7500000000000000000 ) ) ;
#13946=EDGE_LOOP ( 'NONE', ( #66929, #39714, #61449 ) ) ;
#13965=CARTESIAN_POINT ( 'NONE',  ( 3.000000000000000444, 3.673940397442059868E-16, 52.50000000000000000 ) ) ;
#14096=ORIENTED_EDGE ( 'NONE', *, *, #26703, .T. ) ;
#14125=LINE ( 'NONE', #25689, #16097 ) ;
#14221=LINE ( 'NONE', #31073, #50745 ) ;
#14406=CARTESIAN_POINT ( 'NONE',  ( -4.041451884327381450, 7.000000000000006217, 7.500000000000000000 ) ) ;
#14739=ORIENTED_EDGE ( 'NONE', *, *, #18275, .F. ) ;
#14766=EDGE_LOOP ( 'NONE', ( #12432, #41926, #7662, #55234, #54302 ) ) ;
#15053=CARTESIAN_POINT ( 'NONE',  ( 0.000000000000000000, -7.000000000000000888, 0.000000000000000000 ) ) ;
#15211=LINE ( 'NONE', #62999, #47228 ) ;
#15217=FILL_AREA_STYLE ('',( #48618 ) ) ;
#15387=EDGE_CURVE ( 'NONE', #52121, #26743, #1075, .T. ) ;
#15488=ORIENTED_EDGE ( 'NONE', *, *, #31834, .T. ) ;
#15549=CARTESIAN_POINT ( 'NONE',  ( -0.3545099074454313715, 7.000000000000007994, -2.047617446692545640E-14 ) ) ;
#16097=VECTOR ( 'NONE', #62988, 1000.000000000000000 ) ;
#16184=ORIENTED_EDGE ( 'NONE', *, *, #4048, .F. ) ;
#16438=ADVANCED_FACE ( 'NONE', ( #3083 ), #61511, .T. ) ;
#16475=FACE_OUTER_BOUND ( 'NONE', #50692, .T. ) ;
#16476=CARTESIAN_POINT ( 'NONE',  ( 5.000000000000000000, 6.123233995736766282E-16, 0.7500000000000000000 ) ) ;
#16554=LINE ( 'NONE', #1670, #19794 ) ;
#16565=CIRCLE ( 'NONE', #13192, 0.2500000000000000000 ) ;
#16631=ORIENTED_EDGE ( 'NONE', *, *, #29025, .F. ) ;
#16767=CARTESIAN_POINT ( 'NONE',  ( -5.000000000000000000, 0.000000000000000000, 0.7500000000000000000 ) ) ;
#16793=DIRECTION ( 'NONE',  ( 0.000000000000000000, 0.000000000000000000, 1.000000000000000000 ) ) ;
#17040=AXIS2_PLACEMENT_3D ( 'NONE', #63126, #30754, #31800 ) ;
#17330=VERTEX_POINT ( 'NONE', #38845 ) ;
#17485=ORIENTED_EDGE ( 'NONE', *, *, #65521, .T. ) ;
#17493=DIRECTION ( 'NONE',  ( 1.000000000000000000, 0.000000000000000000, 0.000000000000000000 ) ) ;
#17515=DIRECTION ( 'NONE',  ( -0.000000000000000000, -0.000000000000000000, -1.000000000000000000 ) ) ;
#17566=FACE_OUTER_BOUND ( 'NONE', #52102, .T. ) ;
#17568=EDGE_LOOP ( 'NONE', ( #51618, #23131, #6600 ) ) ;
#17768=FACE_OUTER_BOUND ( 'NONE', #59642, .T. ) ;
#17786=SHAPE_DEFINITION_REPRESENTATION ( #63622, #46015 ) ;
#17869=EDGE_CURVE ( 'NONE', #18515, #22486, #54071, .T. ) ;
#17906=AXIS2_PLACEMENT_3D ( 'NONE', #59668, #1573, #17493 ) ;
#17907=ORIENTED_EDGE ( 'NONE', *, *, #28091, .F. ) ;
#17949=ADVANCED_FACE ( 'NONE', ( #51641 ), #38363, .F. ) ;
#17954=MECHANICAL_DESIGN_GEOMETRIC_PRESENTATION_REPRESENTATION('',(#18003),#40529);
#17965=VERTEX_POINT ( 'NONE', #41121 ) ;
#18003=STYLED_ITEM ( 'NONE', ( #4121 ), #59305 ) ;
#18004=CARTESIAN_POINT ( 'NONE',  ( 8.082903768654762899, -1.105959442090949618E-15, 7.500000000000000000 ) ) ;
#18014=AXIS2_PLACEMENT_3D ( 'NONE', #55893, #56935, #13312 ) ;
#18035=PRODUCT_DEFINITION_FORMATION_WITH_SPECIFIED_SOURCE ( 'ANY', '', #51816, .NOT_KNOWN. ) ;
#18275=EDGE_CURVE ( 'NONE', #56480, #32986, #10318, .T. ) ;
#18277=CARTESIAN_POINT ( 'NONE',  ( -8.082903768654762899, 3.516382302766490365E-15, 7.500000000000000000 ) ) ;
#18494=PRESENTATION_STYLE_ASSIGNMENT (( #66314 ) ) ;
#18504=ORIENTED_EDGE ( 'NONE', *, *, #58628, .T. ) ;
#18515=VERTEX_POINT ( 'NONE', #51399 ) ;
#18572=CARTESIAN_POINT ( 'NONE',  ( 4.683753779217433078, -5.887500484252664812, 0.4948905776603311213 ) ) ;
#18656=CARTESIAN_POINT ( 'NONE',  ( 4.041451884327379673, -7.000000000000002665, 7.500000000000000000 ) ) ;
#18788=CARTESIAN_POINT ( 'NONE',  ( 4.041451884327376121, 7.000000000000007105, 7.500000000000000000 ) ) ;
#18856=VECTOR ( 'NONE', #25021, 1000.000000000000000 ) ;
#18883=EDGE_CURVE ( 'NONE', #10139, #12300, #24546, .T. ) ;
#19490=CARTESIAN_POINT ( 'NONE',  ( 0.000000000000000000, -7.000000000000000888, 0.000000000000000000 ) ) ;
#19521=ADVANCED_FACE ( 'NONE', ( #32517 ), #58760, .T. ) ;
#19723=EDGE_LOOP ( 'NONE', ( #42717, #66095, #1767, #51398 ) ) ;
#19794=VECTOR ( 'NONE', #44680, 1000.000000000000114 ) ;
#20285=CARTESIAN_POINT ( 'NONE',  ( 4.041451884327379673, -7.000000000000002665, 1.082903768654758903 ) ) ;
#20434=EDGE_CURVE ( 'NONE', #12490, #583, #53653, .T. ) ;
#20556=B_SPLINE_CURVE_WITH_KNOTS ( 'NONE', 3,
 ( #20285, #5141, #54024, #5827, #4430, #48454, #63208, #15053 ),
 .UNSPECIFIED., .F., .F.,
 ( 4, 2, 2, 4 ),
 ( 0.004248627969284164696, 0.005296391997195108725, 0.006344156025106052754, 0.008439684080927939078 ),
 .UNSPECIFIED. ) ;
#20627=AXIS2_PLACEMENT_3D ( 'NONE', #44248, #23422, #22752 ) ;
#20810=SHAPE_REPRESENTATION_RELATIONSHIP ( 'NONE' , 'NONE' ,  #46015, #57167 ) ;
#20840=DIRECTION ( 'NONE',  ( -0.000000000000000000, -0.000000000000000000, -1.000000000000000000 ) ) ;
#20864=CARTESIAN_POINT ( 'NONE',  ( 0.000000000000000000, 0.000000000000000000, 0.000000000000000000 ) ) ;
#20920=EDGE_CURVE ( 'NONE', #8229, #25042, #67369, .T. ) ;
#21040=DIRECTION ( 'NONE',  ( -1.000000000000000000, -1.073081856240828566E-16, 0.000000000000000000 ) ) ;
#21106=CARTESIAN_POINT ( 'NONE',  ( 0.000000000000000000, 0.000000000000000000, 52.50000000000000000 ) ) ;
#21121=ORIENTED_EDGE ( 'NONE', *, *, #20920, .F. ) ;
#21234=PLANE ( 'NONE',  #17040 ) ;
#21306=FACE_OUTER_BOUND ( 'NONE', #12161, .T. ) ;
#21353=CARTESIAN_POINT ( 'NONE',  ( 0.000000000000000000, 0.000000000000000000, 0.000000000000000000 ) ) ;
#21498=DIRECTION ( 'NONE',  ( 0.000000000000000000, 0.000000000000000000, -1.000000000000000000 ) ) ;
#21532=PRESENTATION_STYLE_ASSIGNMENT (( #65121 ) ) ;
#21590=EDGE_CURVE ( 'NONE', #22068, #52357, #37238, .T. ) ;
#21706=DIRECTION ( 'NONE',  ( 0.000000000000000000, 0.000000000000000000, -1.000000000000000000 ) ) ;
#21744=CARTESIAN_POINT ( 'NONE',  ( 7.441974819423175624, -1.110121504110839430, 0.4967607073414704866 ) ) ;
#21751=VERTEX_POINT ( 'NONE', #60171 ) ;
#21815=DIRECTION ( 'NONE',  ( 0.000000000000000000, 0.000000000000000000, -1.000000000000000000 ) ) ;
#21853=EDGE_LOOP ( 'NONE', ( #62611, #45085, #17485, #25262 ) ) ;
#21998=DIRECTION ( 'NONE',  ( 0.000000000000000000, 0.000000000000000000, 1.000000000000000000 ) ) ;
#22056=DIRECTION ( 'NONE',  ( -1.224646799147353207E-16, 1.000000000000000000, 0.000000000000000000 ) ) ;
#22068=VERTEX_POINT ( 'NONE', #6592 ) ;
#22117=VECTOR ( 'NONE', #44757, 1000.000000000000000 ) ;
#22231=UNCERTAINTY_MEASURE_WITH_UNIT (LENGTH_MEASURE( 1.000000000000000082E-05 ), #10979, 'distance_accuracy_value', 'NONE');
#22269=ORIENTED_EDGE ( 'NONE', *, *, #49273, .F. ) ;
#22430=B_SPLINE_CURVE_WITH_KNOTS ( 'NONE', 3,
 ( #46137, #41211, #3853, #61558, #67925, #57348, #9179, #25338 ),
 .UNSPECIFIED., .F., .F.,
 ( 4, 2, 2, 4 ),
 ( 2.544316211735830308E-07, 0.002094919859796804274, 0.003142252573884619406, 0.004189585287972434971 ),
 .UNSPECIFIED. ) ;
#22432=CARTESIAN_POINT ( 'NONE',  ( 6.062177826491071286, -3.500000000000002220, 0.000000000000000000 ) ) ;
#22466=ADVANCED_FACE ( 'NONE', ( #23756 ), #1267, .F. ) ;
#22486=VERTEX_POINT ( 'NONE', #4986 ) ;
#22520=DIRECTION ( 'NONE',  ( 0.000000000000000000, 0.000000000000000000, -1.000000000000000000 ) ) ;
#22528=AXIS2_PLACEMENT_3D ( 'NONE', #35820, #25587, #51307 ) ;
#22533=CARTESIAN_POINT ( 'NONE',  ( -3.414918479307655907, 7.000000000000006217, 0.7696370661449007944 ) ) ;
#22575=ORIENTED_EDGE ( 'NONE', *, *, #43880, .T. ) ;
#22602=CARTESIAN_POINT ( 'NONE',  ( 2.418535808707042101, 7.000000000000006217, 0.3989014552058406382 ) ) ;
#22752=DIRECTION ( 'NONE',  ( -1.000000000000000000, 0.000000000000000000, 0.000000000000000000 ) ) ;
#22789=CARTESIAN_POINT ( 'NONE',  ( 6.239160159721276244, -3.193457606803200566, 4.616329562535936848E-16 ) ) ;
#22872=DIRECTION ( 'NONE',  ( -1.000000000000000000, 0.000000000000000000, 0.000000000000000000 ) ) ;
#22879=CARTESIAN_POINT ( 'NONE',  ( -7.000000000000002665, 0.000000000000000000, 0.000000000000000000 ) ) ;
#22942=FACE_OUTER_BOUND ( 'NONE', #59672, .T. ) ;
#22953=CARTESIAN_POINT ( 'NONE',  ( 5.000000000000000000, 6.123233995736766282E-16, 0.2499999999999941436 ) ) ;
#23033=ORIENTED_EDGE ( 'NONE', *, *, #55827, .T. ) ;
#23044=ADVANCED_FACE ( 'NONE', ( #17566 ), #39030, .F. ) ;
#23066=ADVANCED_FACE ( 'NONE', ( #56542 ), #67108, .F. ) ;
#23131=ORIENTED_EDGE ( 'NONE', *, *, #21590, .F. ) ;
#23264=COLOUR_RGB ( '', 0.40784314, 0.44705882, 0.49803922) ;
#23314=AXIS2_PLACEMENT_3D ( 'NONE', #3613, #41323, #3259 ) ;
#23400=( NAMED_UNIT ( * ) PLANE_ANGLE_UNIT ( ) SI_UNIT ( $, .RADIAN. ) );
#23409=EDGE_LOOP ( 'NONE', ( #632, #46994 ) ) ;
#23422=DIRECTION ( 'NONE',  ( 0.000000000000000000, 0.000000000000000000, 1.000000000000000000 ) ) ;
#23430=DIRECTION ( 'NONE',  ( -0.5000000000000003331, -0.8660254037844384856, 0.000000000000000000 ) ) ;
#23479=CARTESIAN_POINT ( 'NONE',  ( 4.041451884327379673, -7.000000000000002665, 1.082903768654758903 ) ) ;
#23480=FACE_OUTER_BOUND ( 'NONE', #62058, .T. ) ;
#23492=ORIENTED_EDGE ( 'NONE', *, *, #65183, .F. ) ;
#23576=ORIENTED_EDGE ( 'NONE', *, *, #15387, .T. ) ;
#23656=VERTEX_POINT ( 'NONE', #52609 ) ;
#23703=DIRECTION ( 'NONE',  ( 0.000000000000000000, 0.000000000000000000, 1.000000000000000000 ) ) ;
#23756=FACE_OUTER_BOUND ( 'NONE', #21853, .T. ) ;
#24001=VERTEX_POINT ( 'NONE', #6333 ) ;
#24082=VECTOR ( 'NONE', #45428, 1000.000000000000000 ) ;
#24120=VERTEX_POINT ( 'NONE', #22879 ) ;
#24221=EDGE_LOOP ( 'NONE', ( #2081, #7598, #43054, #44031 ) ) ;
#24234=CARTESIAN_POINT ( 'NONE',  ( -3.000000000000000444, 0.000000000000000000, 52.50000000000000000 ) ) ;
#24449=CIRCLE ( 'NONE', #23314, 3.000000000000000444 ) ;
#24453=ORIENTED_EDGE ( 'NONE', *, *, #11903, .F. ) ;
#24546=LINE ( 'NONE', #46061, #174 ) ;
#24891=DIRECTION ( 'NONE',  ( -1.000000000000000000, 0.000000000000000000, 0.000000000000000000 ) ) ;
#24901=SURFACE_STYLE_USAGE ( .BOTH. , #57982 ) ;
#24939=DIRECTION ( 'NONE',  ( -1.000000000000000000, 0.000000000000000000, 0.000000000000000000 ) ) ;
#25021=DIRECTION ( 'NONE',  ( -0.000000000000000000, -0.000000000000000000, -1.000000000000000000 ) ) ;
#25042=VERTEX_POINT ( 'NONE', #626 ) ;
#25124=CARTESIAN_POINT ( 'NONE',  ( 7.766391886667110889, 0.5482146608018589884, 0.7663918866669823249 ) ) ;
#25166=CARTESIAN_POINT ( 'NONE',  ( -6.413663052920317575, -2.891209729714697030, 1.212104147520903391E-15 ) ) ;
#25262=ORIENTED_EDGE ( 'NONE', *, *, #60865, .F. ) ;
#25338=CARTESIAN_POINT ( 'NONE',  ( -6.062177826491071286, 3.500000000000000888, 0.000000000000000000 ) ) ;
#25341=CARTESIAN_POINT ( 'NONE',  ( -6.062177826491072175, -3.499999999999998668, 0.000000000000000000 ) ) ;
#25405=CARTESIAN_POINT ( 'NONE',  ( -4.041451884327381450, 7.000000000000006217, 1.082903768654761345 ) ) ;
#25587=DIRECTION ( 'NONE',  ( 0.000000000000000000, 0.000000000000000000, -1.000000000000000000 ) ) ;
#25672=CARTESIAN_POINT ( 'NONE',  ( -5.185928986913077132, -5.017707510222358280, 0.2088670156639313991 ) ) ;
#25689=CARTESIAN_POINT ( 'NONE',  ( 5.000000000000000000, 6.123233995736766282E-16, 1.000000000000000000 ) ) ;
#25888=CONICAL_SURFACE ( 'NONE', #45029, 7.000000000000000888, 0.7853981633974500554 ) ;
#26018=CARTESIAN_POINT ( 'NONE',  ( -4.682380833558966948, -5.889878495889163013, 0.4967607073414698760 ) ) ;
#26173=FACE_OUTER_BOUND ( 'NONE', #3831, .T. ) ;
#26513=CIRCLE ( 'NONE', #65855, 5.000000000000000000 ) ;
#26520=FACE_BOUND ( 'NONE', #53047, .T. ) ;
#26547=DIRECTION ( 'NONE',  ( -0.000000000000000000, -0.000000000000000000, -1.000000000000000000 ) ) ;
#26703=EDGE_CURVE ( 'NONE', #10139, #8806, #65669, .T. ) ;
#26743=VERTEX_POINT ( 'NONE', #56142 ) ;
#26756=CARTESIAN_POINT ( 'NONE',  ( 4.358330484967979146, 6.451150163859158404, 0.7660251680141578756 ) ) ;
#26951=FACE_OUTER_BOUND ( 'NONE', #17568, .T. ) ;
#27102=CARTESIAN_POINT ( 'NONE',  ( 5.185928986913072691, 5.017707510222363609, 0.2088670156639309550 ) ) ;
#27127=SURFACE_SIDE_STYLE ('',( #54576 ) ) ;
#27141=DIRECTION ( 'NONE',  ( -1.000000000000000000, 0.000000000000000000, 0.000000000000000000 ) ) ;
#27197=ADVANCED_FACE ( 'NONE', ( #17768 ), #47727, .T. ) ;
#27427=DIRECTION ( 'NONE',  ( 1.000000000000000000, 0.000000000000000000, 0.000000000000000000 ) ) ;
#27502=ORIENTED_EDGE ( 'NONE', *, *, #64592, .T. ) ;
#27544=ORIENTED_EDGE ( 'NONE', *, *, #30980, .T. ) ;
#27631=VERTEX_POINT ( 'NONE', #37271 ) ;
#27637=DIRECTION ( 'NONE',  ( 1.000000000000000000, 0.000000000000000000, 0.000000000000000000 ) ) ;
#27651=PLANE ( 'NONE',  #63678 ) ;
#27708=LINE ( 'NONE', #43615, #2021 ) ;
#28091=EDGE_CURVE ( 'NONE', #53965, #38934, #85, .T. ) ;
#28095=STYLED_ITEM ( 'NONE', ( #58103 ), #57167 ) ;
#28180=CARTESIAN_POINT ( 'NONE',  ( 2.755511676787084419, 7.000000000000007105, 0.5168645644872258416 ) ) ;
#28381=ORIENTED_EDGE ( 'NONE', *, *, #10289, .T. ) ;
#28508=ORIENTED_EDGE ( 'NONE', *, *, #18883, .T. ) ;
#28611=DIRECTION ( 'NONE',  ( 0.5000000000000001110, 0.8660254037844385966, 0.000000000000000000 ) ) ;
#28811=CARTESIAN_POINT ( 'NONE',  ( 0.000000000000000000, 0.000000000000000000, 1.000000000000000000 ) ) ;
#28889=CARTESIAN_POINT ( 'NONE',  ( 3.409623619629272184, 7.000000000000006217, 0.7804846576204730324 ) ) ;
#28960=VERTEX_POINT ( 'NONE', #18004 ) ;
#29025=EDGE_CURVE ( 'NONE', #7949, #11857, #14125, .T. ) ;
#29144=AXIS2_PLACEMENT_3D ( 'NONE', #46238, #62376, #27141 ) ;
#29166=CARTESIAN_POINT ( 'NONE',  ( 0.000000000000000000, 0.000000000000000000, 0.2499999999999941436 ) ) ;
#29220=MECHANICAL_DESIGN_GEOMETRIC_PRESENTATION_REPRESENTATION('',(#28095),#37119);
#29346=CARTESIAN_POINT ( 'NONE',  ( -3.414918479307654575, -7.000000000000001776, 0.7696370661448970196 ) ) ;
#29390=CARTESIAN_POINT ( 'NONE',  ( -8.082903768654762899, 3.463586619550771876E-15, 1.082903768654759125 ) ) ;
#29463=EDGE_CURVE ( 'NONE', #12490, #11857, #12689, .T. ) ;
#29487=AXIS2_PLACEMENT_3D ( 'NONE', #63544, #36143, #41783 ) ;
#29525=DIRECTION ( 'NONE',  ( -0.000000000000000000, -0.000000000000000000, -1.000000000000000000 ) ) ;
#29586=ORIENTED_EDGE ( 'NONE', *, *, #31239, .F. ) ;
#29724=ORIENTED_EDGE ( 'NONE', *, *, #67498, .T. ) ;
#29845=CARTESIAN_POINT ( 'NONE',  ( -3.000000000000000444, 0.000000000000000000, 7.500000000000000000 ) ) ;
#29981=CIRCLE ( 'NONE', #17906, 3.000000000000000444 ) ;
#30045=CARTESIAN_POINT ( 'NONE',  ( 6.062177826491070398, 3.500000000000002665, 0.000000000000000000 ) ) ;
#30455=UNCERTAINTY_MEASURE_WITH_UNIT (LENGTH_MEASURE( 1.000000000000000082E-05 ), #37729, 'distance_accuracy_value', 'NONE');
#30491=VERTEX_POINT ( 'NONE', #45434 ) ;
#30754=DIRECTION ( 'NONE',  ( 0.000000000000000000, 0.000000000000000000, 1.000000000000000000 ) ) ;
#30908=CARTESIAN_POINT ( 'NONE',  ( 0.000000000000000000, 0.000000000000000000, 52.50000000000000000 ) ) ;
#30947=DIRECTION ( 'NONE',  ( -0.000000000000000000, -0.000000000000000000, -1.000000000000000000 ) ) ;
#30980=EDGE_CURVE ( 'NONE', #56480, #30491, #7494, .T. ) ;
#30997=( LENGTH_UNIT ( ) NAMED_UNIT ( * ) SI_UNIT ( .MILLI., .METRE. ) );
#31073=CARTESIAN_POINT ( 'NONE',  ( -4.041451884327381450, -7.000000000000002665, 7.500000000000000000 ) ) ;
#31076=VECTOR ( 'NONE', #26547, 1000.000000000000000 ) ;
#31227=CARTESIAN_POINT ( 'NONE',  ( -5.000000000000000000, 0.000000000000000000, 0.2499999999999941436 ) ) ;
#31239=EDGE_CURVE ( 'NONE', #24120, #57001, #67243, .T. ) ;
#31458=ORIENTED_EDGE ( 'NONE', *, *, #15387, .F. ) ;
#31551=DIRECTION ( 'NONE',  ( 0.000000000000000000, 0.000000000000000000, -1.000000000000000000 ) ) ;
#31671=( GEOMETRIC_REPRESENTATION_CONTEXT ( 3 ) GLOBAL_UNCERTAINTY_ASSIGNED_CONTEXT ( ( #60273 ) ) GLOBAL_UNIT_ASSIGNED_CONTEXT ( ( #2943, #23400, #61378 ) ) REPRESENTATION_CONTEXT ( 'NONE', 'WORKASPACE' ) );
#31723=ORIENTED_EDGE ( 'NONE', *, *, #4048, .T. ) ;
#31763=CONICAL_SURFACE ( 'NONE', #2491, 7.000000000000000888, 0.7853981633974500554 ) ;
#31800=DIRECTION ( 'NONE',  ( 1.000000000000000000, 0.000000000000000000, -0.000000000000000000 ) ) ;
#31825=LINE ( 'NONE', #63161, #31076 ) ;
#31834=EDGE_CURVE ( 'NONE', #24001, #56480, #42667, .T. ) ;
#31882=CARTESIAN_POINT ( 'NONE',  ( -8.082903768654762899, 3.516382302766490365E-15, 7.500000000000000000 ) ) ;
#32007=DIRECTION ( 'NONE',  ( 1.000000000000000000, 0.000000000000000000, 0.000000000000000000 ) ) ;
#32135=ORIENTED_EDGE ( 'NONE', *, *, #9733, .F. ) ;
#32234=LINE ( 'NONE', #31882, #54534 ) ;
#32388=CARTESIAN_POINT ( 'NONE',  ( 4.041451884327376121, 7.000000000000007105, 1.082903768654759569 ) ) ;
#32422=DIRECTION ( 'NONE',  ( 0.000000000000000000, -0.000000000000000000, 1.000000000000000000 ) ) ;
#32517=FACE_OUTER_BOUND ( 'NONE', #44407, .T. ) ;
#32732=CARTESIAN_POINT ( 'NONE',  ( -4.041451884327381450, 7.000000000000006217, 1.082903768654761345 ) ) ;
#32771=LINE ( 'NONE', #34499, #22117 ) ;
#32986=VERTEX_POINT ( 'NONE', #51427 ) ;
#33062=ORIENTED_EDGE ( 'NONE', *, *, #21590, .T. ) ;
#33141=FILL_AREA_STYLE_COLOUR ( '', #23264 ) ;
#33315=FACE_OUTER_BOUND ( 'NONE', #14766, .T. ) ;
#33411=CARTESIAN_POINT ( 'NONE',  ( 5.000000000000000000, 6.123233995736766282E-16, 0.2499999999999941436 ) ) ;
#33490=ADVANCED_FACE ( 'NONE', ( #21306 ), #25888, .T. ) ;
#33786=ORIENTED_EDGE ( 'NONE', *, *, #58702, .F. ) ;
#34006=CIRCLE ( 'NONE', #29487, 5.000000000000000000 ) ;
#34101=LINE ( 'NONE', #33411, #42721 ) ;
#34452=STYLED_ITEM ( 'NONE', ( #21532 ), #3590 ) ;
#34499=CARTESIAN_POINT ( 'NONE',  ( -8.082903768654762899, 3.516382302766490365E-15, 7.500000000000000000 ) ) ;
#34527=CARTESIAN_POINT ( 'NONE',  ( -7.511572993685801073E-16, 7.000000000000000888, 0.000000000000000000 ) ) ;
#34554=AXIS2_PLACEMENT_3D ( 'NONE', #34976, #67332, #51496 ) ;
#34759=EDGE_CURVE ( 'NONE', #30491, #22486, #20556, .T. ) ;
#34805=CARTESIAN_POINT ( 'NONE',  ( 0.000000000000000000, 0.000000000000000000, 7.500000000000000000 ) ) ;
#34973=CARTESIAN_POINT ( 'NONE',  ( -5.000000000000000000, 0.000000000000000000, 1.000000000000000000 ) ) ;
#34976=CARTESIAN_POINT ( 'NONE',  ( 0.000000000000000000, 0.000000000000000000, 0.000000000000000000 ) ) ;
#35083=EDGE_LOOP ( 'NONE', ( #41605, #43162, #40093 ) ) ;
#35090=ADVANCED_FACE ( 'NONE', ( #26520, #26173 ), #21234, .T. ) ;
#35513=UNCERTAINTY_MEASURE_WITH_UNIT (LENGTH_MEASURE( 1.000000000000000082E-05 ), #8407, 'distance_accuracy_value', 'NONE');
#35626=ORIENTED_EDGE ( 'NONE', *, *, #13164, .F. ) ;
#35632=CARTESIAN_POINT ( 'NONE',  ( 0.000000000000000000, 0.000000000000000000, 52.50000000000000000 ) ) ;
#35669=AXIS2_PLACEMENT_3D ( 'NONE', #5164, #47814, #10470 ) ;
#35692=CARTESIAN_POINT ( 'NONE',  ( -1.744870598150811469, -7.000000000000001776, 0.2069669095365348765 ) ) ;
#35734=EDGE_LOOP ( 'NONE', ( #31458, #23033, #46968, #41698 ) ) ;
#35805=FACE_OUTER_BOUND ( 'NONE', #19723, .T. ) ;
#35807=EDGE_LOOP ( 'NONE', ( #40146, #67184, #44614, #14096, #6234 ) ) ;
#35820=CARTESIAN_POINT ( 'NONE',  ( 0.000000000000000000, 0.000000000000000000, 0.7500000000000000000 ) ) ;
#35890=ORIENTED_EDGE ( 'NONE', *, *, #69104, .T. ) ;
#35910=ADVANCED_FACE ( 'NONE', ( #58140 ), #31763, .T. ) ;
#36129=AXIS2_PLACEMENT_3D ( 'NONE', #4111, #3397, #24891 ) ;
#36143=DIRECTION ( 'NONE',  ( -0.000000000000000000, -0.000000000000000000, 1.000000000000000000 ) ) ;
#36212=EDGE_CURVE ( 'NONE', #23656, #18515, #1914, .T. ) ;
#36274=FACE_OUTER_BOUND ( 'NONE', #50328, .T. ) ;
#36287=CARTESIAN_POINT ( 'NONE',  ( -4.041451884327381450, -7.000000000000002665, 1.082903768654759791 ) ) ;
#36324=SURFACE_STYLE_USAGE ( .BOTH. , #37023 ) ;
#36680=DIRECTION ( 'NONE',  ( -0.5000000000000003331, 0.8660254037844383745, 0.000000000000000000 ) ) ;
#36683=SURFACE_STYLE_FILL_AREA ( #15217 ) ;
#36694=ORIENTED_EDGE ( 'NONE', *, *, #20434, .T. ) ;
#36712=CARTESIAN_POINT ( 'NONE',  ( -5.365183871890746303, 4.707228941936129729, 0.1074872947962681735 ) ) ;
#36883=DIRECTION ( 'NONE',  ( 0.000000000000000000, 0.000000000000000000, 1.000000000000000000 ) ) ;
#37023=SURFACE_SIDE_STYLE ('',( #36683 ) ) ;
#37039=EDGE_LOOP ( 'NONE', ( #68200, #33786, #48523, #63346 ) ) ;
#37119=( GEOMETRIC_REPRESENTATION_CONTEXT ( 3 ) GLOBAL_UNCERTAINTY_ASSIGNED_CONTEXT ( ( #30455 ) ) GLOBAL_UNIT_ASSIGNED_CONTEXT ( ( #37729, #52829, #69673 ) ) REPRESENTATION_CONTEXT ( 'NONE', 'WORKASPACE' ) );
#37238=CIRCLE ( 'NONE', #52927, 7.000000000000000888 ) ;
#37271=CARTESIAN_POINT ( 'NONE',  ( 4.041451884327376121, 7.000000000000007105, 7.500000000000000000 ) ) ;
#37379=ADVANCED_FACE ( 'NONE', ( #2171 ), #12439, .T. ) ;
#37563=CARTESIAN_POINT ( 'NONE',  ( 0.000000000000000000, 0.000000000000000000, 0.000000000000000000 ) ) ;
#37722=CARTESIAN_POINT ( 'NONE',  ( 0.000000000000000000, 0.000000000000000000, 0.000000000000000000 ) ) ;
#37729=( LENGTH_UNIT ( ) NAMED_UNIT ( * ) SI_UNIT ( .MILLI., .METRE. ) );
#37748=CARTESIAN_POINT ( 'NONE',  ( 5.705565085145811288, 4.117671386636414077, 0.02778322089669325520 ) ) ;
#37981=CIRCLE ( 'NONE', #34554, 5.249999999999991118 ) ;
#38109=PLANE ( 'NONE',  #61330 ) ;
#38184=ORIENTED_EDGE ( 'NONE', *, *, #38491, .F. ) ;
#38203=DIRECTION ( 'NONE',  ( -1.000000000000000000, 0.000000000000000000, 0.000000000000000000 ) ) ;
#38276=DIRECTION ( 'NONE',  ( -1.000000000000000000, -1.224646799147353454E-16, 0.000000000000000000 ) ) ;
#38363=CONICAL_SURFACE ( 'NONE', #36129, 5.000000000000000000, 0.7853981633974415066 ) ;
#38374=ORIENTED_EDGE ( 'NONE', *, *, #53152, .F. ) ;
#38491=EDGE_CURVE ( 'NONE', #21751, #30491, #61206, .T. ) ;
#38575=DIRECTION ( 'NONE',  ( -0.7071067811865426878, 0.000000000000000000, -0.7071067811865524577 ) ) ;
#38591=AXIS2_PLACEMENT_3D ( 'NONE', #63903, #31551, #41815 ) ;
#38695=ORIENTED_EDGE ( 'NONE', *, *, #26703, .F. ) ;
#38845=CARTESIAN_POINT ( 'NONE',  ( -4.041451884327381450, -7.000000000000002665, 7.500000000000000000 ) ) ;
#38934=VERTEX_POINT ( 'NONE', #65541 ) ;
#39030=PLANE ( 'NONE',  #1380 ) ;
#39070=AXIS2_PLACEMENT_3D ( 'NONE', #54485, #11234, #53790 ) ;
#39218=CARTESIAN_POINT ( 'NONE',  ( -4.041451884327381450, 7.000000000000006217, 7.500000000000000000 ) ) ;
#39233=DIRECTION ( 'NONE',  ( 1.073081856240828566E-16, -1.000000000000000000, 0.000000000000000000 ) ) ;
#39281=ORIENTED_EDGE ( 'NONE', *, *, #51391, .F. ) ;
#39367=COLOUR_RGB ( '', 0.08235294, 0.09019608, 0.10196078) ;
#39623=DIRECTION ( 'NONE',  ( -1.000000000000000000, 0.000000000000000000, 0.000000000000000000 ) ) ;
#39714=ORIENTED_EDGE ( 'NONE', *, *, #36212, .T. ) ;
#39822=AXIS2_PLACEMENT_3D ( 'NONE', #54737, #11146, #23430 ) ;
#39879=ORIENTED_EDGE ( 'NONE', *, *, #29463, .T. ) ;
#40054=CARTESIAN_POINT ( 'NONE',  ( 5.365183871890743639, -4.707228941936128841, 0.1074872947962652175 ) ) ;
#40068=DIRECTION ( 'NONE',  ( -0.8660254037844384856, -0.5000000000000004441, 0.000000000000000000 ) ) ;
#40093=ORIENTED_EDGE ( 'NONE', *, *, #11903, .T. ) ;
#40146=ORIENTED_EDGE ( 'NONE', *, *, #55186, .F. ) ;
#40188=DIRECTION ( 'NONE',  ( -0.7071067811865487940, 0.000000000000000000, 0.7071067811865463515 ) ) ;
#40382=CARTESIAN_POINT ( 'NONE',  ( 0.000000000000000000, 0.000000000000000000, 0.000000000000000000 ) ) ;
#40408=CARTESIAN_POINT ( 'NONE',  ( 0.000000000000000000, 0.000000000000000000, 0.000000000000000000 ) ) ;
#40528=EDGE_CURVE ( 'NONE', #12300, #57001, #32771, .T. ) ;
#40529=( GEOMETRIC_REPRESENTATION_CONTEXT ( 3 ) GLOBAL_UNCERTAINTY_ASSIGNED_CONTEXT ( ( #35513 ) ) GLOBAL_UNIT_ASSIGNED_CONTEXT ( ( #8407, #68527, #67840 ) ) REPRESENTATION_CONTEXT ( 'NONE', 'WORKASPACE' ) );
#40633=B_SPLINE_CURVE_WITH_KNOTS ( 'NONE', 3,
 ( #7945, #25166, #8312, #2623, #66696, #29390 ),
 .UNSPECIFIED., .F., .F.,
 ( 4, 2, 4 ),
 ( 0.004189585287972440175, 0.006269578072783814175, 0.008349570857595188175 ),
 .UNSPECIFIED. ) ;
#40808=AXIS2_PLACEMENT_3D ( 'NONE', #49100, #21998, #38203 ) ;
#40855=ADVANCED_FACE ( 'NONE', ( #36274 ), #56292, .F. ) ;
#40994=CARTESIAN_POINT ( 'NONE',  ( -0.3545099074454303167, -7.000000000000004441, -2.440407800158045118E-14 ) ) ;
#41102=ORIENTED_EDGE ( 'NONE', *, *, #60865, .T. ) ;
#41121=CARTESIAN_POINT ( 'NONE',  ( 4.041451884327376121, 7.000000000000007105, 1.082903768654759569 ) ) ;
#41131=SURFACE_STYLE_FILL_AREA ( #46781 ) ;
#41211=CARTESIAN_POINT ( 'NONE',  ( -7.766025168014158986, 0.5488498361408529203, 0.7660251680141585418 ) ) ;
#41323=DIRECTION ( 'NONE',  ( 0.000000000000000000, 0.000000000000000000, 1.000000000000000000 ) ) ;
#41325=EDGE_LOOP ( 'NONE', ( #17907, #28381, #29724, #1963 ) ) ;
#41605=ORIENTED_EDGE ( 'NONE', *, *, #9733, .T. ) ;
#41619=FACE_OUTER_BOUND ( 'NONE', #37039, .T. ) ;
#41635=AXIS2_PLACEMENT_3D ( 'NONE', #21353, #48489, #43229 ) ;
#41698=ORIENTED_EDGE ( 'NONE', *, *, #65521, .F. ) ;
#41720=ADVANCED_FACE ( 'NONE', ( #44516 ), #65919, .F. ) ;
#41783=DIRECTION ( 'NONE',  ( -1.000000000000000000, 0.000000000000000000, 0.000000000000000000 ) ) ;
#41810=EDGE_CURVE ( 'NONE', #60935, #7949, #53868, .T. ) ;
#41815=DIRECTION ( 'NONE',  ( -1.000000000000000000, 0.000000000000000000, 0.000000000000000000 ) ) ;
#41926=ORIENTED_EDGE ( 'NONE', *, *, #66986, .F. ) ;
#42027=AXIS2_PLACEMENT_3D ( 'NONE', #48834, #22056, #38276 ) ;
#42150=ORIENTED_EDGE ( 'NONE', *, *, #67498, .F. ) ;
#42165=DIRECTION ( 'NONE',  ( 0.4999999999999997780, -0.8660254037844387076, 0.000000000000000000 ) ) ;
#42303=DIRECTION ( 'NONE',  ( -1.000000000000000000, 0.000000000000000000, 0.000000000000000000 ) ) ;
#42341=CARTESIAN_POINT ( 'NONE',  ( -6.062177826491071286, 3.500000000000000888, 0.000000000000000000 ) ) ;
#42394=( GEOMETRIC_REPRESENTATION_CONTEXT ( 3 ) GLOBAL_UNCERTAINTY_ASSIGNED_CONTEXT ( ( #22231 ) ) GLOBAL_UNIT_ASSIGNED_CONTEXT ( ( #10979, #363, #1409 ) ) REPRESENTATION_CONTEXT ( 'NONE', 'WORKASPACE' ) );
#42667=B_SPLINE_CURVE_WITH_KNOTS ( 'NONE', 3,
 ( #214, #53424, #21744, #59712, #53739, #1257, #22789, #22432 ),
 .UNSPECIFIED., .F., .F.,
 ( 4, 2, 2, 4 ),
 ( 2.544316211736855218E-07, 0.002094919859796806443, 0.003142252573884622875, 0.004189585287972439308 ),
 .UNSPECIFIED. ) ;
#42717=ORIENTED_EDGE ( 'NONE', *, *, #829, .F. ) ;
#42721=VECTOR ( 'NONE', #55558, 1000.000000000000000 ) ;
#42840=AXIS2_PLACEMENT_3D ( 'NONE', #59977, #7217, #49786 ) ;
#42851=ADVANCED_FACE ( 'NONE', ( #12448 ), #12805, .F. ) ;
#43054=ORIENTED_EDGE ( 'NONE', *, *, #829, .T. ) ;
#43162=ORIENTED_EDGE ( 'NONE', *, *, #50290, .T. ) ;
#43229=DIRECTION ( 'NONE',  ( -1.000000000000000000, 0.000000000000000000, 0.000000000000000000 ) ) ;
#43481=EDGE_CURVE ( 'NONE', #11857, #49555, #34101, .T. ) ;
#43545=CIRCLE ( 'NONE', #39070, 5.249999999999991118 ) ;
#43566=EDGE_CURVE ( 'NONE', #38934, #8229, #61497, .T. ) ;
#43615=CARTESIAN_POINT ( 'NONE',  ( 3.000000000000000444, 3.673940397442059868E-16, 52.50000000000000000 ) ) ;
#43803=EDGE_LOOP ( 'NONE', ( #54280, #52279 ) ) ;
#43814=EDGE_CURVE ( 'NONE', #27631, #17965, #61345, .T. ) ;
#43859=CARTESIAN_POINT ( 'NONE',  ( 0.000000000000000000, 0.000000000000000000, 0.000000000000000000 ) ) ;
#43880=EDGE_CURVE ( 'NONE', #60935, #12490, #7211, .T. ) ;
#43905=TOROIDAL_SURFACE ( 'NONE', #22528, 4.750000000000000000, 0.2500000000000000000 ) ;
#44031=ORIENTED_EDGE ( 'NONE', *, *, #43880, .F. ) ;
#44061=ORIENTED_EDGE ( 'NONE', *, *, #43814, .F. ) ;
#44248=CARTESIAN_POINT ( 'NONE',  ( 0.000000000000000000, 0.000000000000000000, 0.000000000000000000 ) ) ;
#44330=VECTOR ( 'NONE', #40188, 1000.000000000000000 ) ;
#44334=CARTESIAN_POINT ( 'NONE',  ( 0.000000000000000000, 0.000000000000000000, 0.2499999999999941436 ) ) ;
#44406=EDGE_CURVE ( 'NONE', #28960, #27631, #15211, .T. ) ;
#44407=EDGE_LOOP ( 'NONE', ( #49679, #15488, #69278 ) ) ;
#44516=FACE_OUTER_BOUND ( 'NONE', #35807, .T. ) ;
#44614=ORIENTED_EDGE ( 'NONE', *, *, #18883, .F. ) ;
#44648=CARTESIAN_POINT ( 'NONE',  ( 4.357963766315031684, -6.451785339198144342, 0.7663918866669806595 ) ) ;
#44680=DIRECTION ( 'NONE',  ( 0.5000000000000003331, 0.8660254037844384856, 0.000000000000000000 ) ) ;
#44757=DIRECTION ( 'NONE',  ( -0.000000000000000000, -0.000000000000000000, -1.000000000000000000 ) ) ;
#44986=DIRECTION ( 'NONE',  ( 0.000000000000000000, 0.000000000000000000, 1.000000000000000000 ) ) ;
#45029=AXIS2_PLACEMENT_3D ( 'NONE', #37563, #48445, #64910 ) ;
#45051=DIRECTION ( 'NONE',  ( 0.000000000000000000, 0.000000000000000000, -1.000000000000000000 ) ) ;
#45085=ORIENTED_EDGE ( 'NONE', *, *, #69104, .F. ) ;
#45232=CARTESIAN_POINT ( 'NONE',  ( 7.440601873764706831, 1.112499515747338741, 0.4948905776603317874 ) ) ;
#45428=DIRECTION ( 'NONE',  ( -0.000000000000000000, -0.000000000000000000, -1.000000000000000000 ) ) ;
#45434=CARTESIAN_POINT ( 'NONE',  ( 4.041451884327379673, -7.000000000000002665, 1.082903768654758903 ) ) ;
#45500=AXIS2_PLACEMENT_3D ( 'NONE', #12812, #63350, #42303 ) ;
#46015=SHAPE_REPRESENTATION ( '13. Bolt M6x45', ( #42840 ), #2196 ) ;
#46020=FACE_BOUND ( 'NONE', #23409, .T. ) ;
#46061=CARTESIAN_POINT ( 'NONE',  ( -4.041451884327381450, 7.000000000000006217, 7.500000000000000000 ) ) ;
#46137=CARTESIAN_POINT ( 'NONE',  ( -8.082903768654762899, 3.463586619550771876E-15, 1.082903768654759125 ) ) ;
#46238=CARTESIAN_POINT ( 'NONE',  ( 0.000000000000000000, 0.000000000000000000, 0.7500000000000000000 ) ) ;
#46301=CARTESIAN_POINT ( 'NONE',  ( 5.249999999999991118, 6.429395695523593306E-16, 0.000000000000000000 ) ) ;
#46605=ADVANCED_FACE ( 'NONE', ( #35805 ), #12662, .F. ) ;
#46637=CARTESIAN_POINT ( 'NONE',  ( -4.041451884327381450, -7.000000000000002665, 1.082903768654759791 ) ) ;
#46781=FILL_AREA_STYLE ('',( #8739 ) ) ;
#46841=CARTESIAN_POINT ( 'NONE',  ( -8.082903768654762899, 3.463586619550771876E-15, 1.082903768654759125 ) ) ;
#46968=ORIENTED_EDGE ( 'NONE', *, *, #41810, .F. ) ;
#46994=ORIENTED_EDGE ( 'NONE', *, *, #67500, .T. ) ;
#47228=VECTOR ( 'NONE', #36680, 1000.000000000000114 ) ;
#47326=VECTOR ( 'NONE', #21040, 1000.000000000000000 ) ;
#47459=DIRECTION ( 'NONE',  ( 1.000000000000000000, 0.000000000000000000, 0.000000000000000000 ) ) ;
#47482=CARTESIAN_POINT ( 'NONE',  ( 4.041451884327376121, 7.000000000000007105, 7.500000000000000000 ) ) ;
#47552=CARTESIAN_POINT ( 'NONE',  ( -5.885195493260865440, -3.806542393196800766, 1.022368767335940312E-15 ) ) ;
#47723=AXIS2_PLACEMENT_3D ( 'NONE', #35632, #20840, #9607 ) ;
#47727=CONICAL_SURFACE ( 'NONE', #45500, 7.000000000000000888, 0.7853981633974500554 ) ;
#47814=DIRECTION ( 'NONE',  ( 0.000000000000000000, 0.000000000000000000, 1.000000000000000000 ) ) ;
#47943=( NAMED_UNIT ( * ) SI_UNIT ( $, .STERADIAN. ) SOLID_ANGLE_UNIT ( ) );
#48079=AXIS2_PLACEMENT_3D ( 'NONE', #56995, #30947, #3845 ) ;
#48316=CIRCLE ( 'NONE', #61746, 4.750000000000000000 ) ;
#48406=AXIS2_PLACEMENT_3D ( 'NONE', #30908, #29525, #24939 ) ;
#48445=DIRECTION ( 'NONE',  ( 0.000000000000000000, 0.000000000000000000, 1.000000000000000000 ) ) ;
#48454=CARTESIAN_POINT ( 'NONE',  ( 1.401671290772266598, -7.000000000000003553, 0.1093172352041265755 ) ) ;
#48486=CIRCLE ( 'NONE', #13634, 7.000000000000001776 ) ;
#48489=DIRECTION ( 'NONE',  ( 0.000000000000000000, 0.000000000000000000, 1.000000000000000000 ) ) ;
#48493=ORIENTED_EDGE ( 'NONE', *, *, #58829, .T. ) ;
#48523=ORIENTED_EDGE ( 'NONE', *, *, #43566, .T. ) ;
#48583=AXIS2_PLACEMENT_3D ( 'NONE', #13275, #40068, #62161 ) ;
#48618=FILL_AREA_STYLE_COLOUR ( '', #65175 ) ;
#48834=CARTESIAN_POINT ( 'NONE',  ( 4.750000000000000000, 5.817072295949927426E-16, 0.7500000000000000000 ) ) ;
#48848=ORIENTED_EDGE ( 'NONE', *, *, #44406, .F. ) ;
#49100=CARTESIAN_POINT ( 'NONE',  ( 0.000000000000000000, 0.000000000000000000, 0.000000000000000000 ) ) ;
#49131=DIRECTION ( 'NONE',  ( 0.000000000000000000, 0.000000000000000000, 1.000000000000000000 ) ) ;
#49259=DIRECTION ( 'NONE',  ( -1.000000000000000000, 0.000000000000000000, 0.000000000000000000 ) ) ;
#49273=EDGE_CURVE ( 'NONE', #12300, #17330, #32234, .T. ) ;
#49555=VERTEX_POINT ( 'NONE', #46301 ) ;
#49679=ORIENTED_EDGE ( 'NONE', *, *, #53152, .T. ) ;
#49737=ORIENTED_EDGE ( 'NONE', *, *, #54189, .F. ) ;
#49786=DIRECTION ( 'NONE',  ( 1.000000000000000000, 0.000000000000000000, 0.000000000000000000 ) ) ;
#49840=CARTESIAN_POINT ( 'NONE',  ( 0.000000000000000000, 0.000000000000000000, 1.000000000000000000 ) ) ;
#50228=MECHANICAL_DESIGN_GEOMETRIC_PRESENTATION_REPRESENTATION('',(#34452),#42394);
#50264=DIRECTION ( 'NONE',  ( 1.000000000000000000, 0.000000000000000000, 0.000000000000000000 ) ) ;
#50290=EDGE_CURVE ( 'NONE', #32986, #52357, #54683, .T. ) ;
#50328=EDGE_LOOP ( 'NONE', ( #16631, #41102, #22575, #39879 ) ) ;
#50483=APPLICATION_CONTEXT ( 'automotive_design' ) ;
#50692=EDGE_LOOP ( 'NONE', ( #35890, #23576 ) ) ;
#50745=VECTOR ( 'NONE', #27427, 1000.000000000000000 ) ;
#51198=DIRECTION ( 'NONE',  ( 0.000000000000000000, 0.000000000000000000, -1.000000000000000000 ) ) ;
#51282=ORIENTED_EDGE ( 'NONE', *, *, #12454, .T. ) ;
#51307=DIRECTION ( 'NONE',  ( -1.000000000000000000, 0.000000000000000000, 0.000000000000000000 ) ) ;
#51308=ORIENTED_EDGE ( 'NONE', *, *, #58628, .F. ) ;
#51348=DIRECTION ( 'NONE',  ( 1.000000000000000000, 0.000000000000000000, 0.000000000000000000 ) ) ;
#51391=EDGE_CURVE ( 'NONE', #8806, #52357, #3380, .T. ) ;
#51398=ORIENTED_EDGE ( 'NONE', *, *, #20434, .F. ) ;
#51399=CARTESIAN_POINT ( 'NONE',  ( -6.062177826491072175, -3.499999999999998668, 0.000000000000000000 ) ) ;
#51413=ORIENTED_EDGE ( 'NONE', *, *, #50290, .F. ) ;
#51427=CARTESIAN_POINT ( 'NONE',  ( 6.062177826491070398, 3.500000000000002665, 0.000000000000000000 ) ) ;
#51496=DIRECTION ( 'NONE',  ( 1.000000000000000000, 0.000000000000000000, 0.000000000000000000 ) ) ;
#51618=ORIENTED_EDGE ( 'NONE', *, *, #51391, .T. ) ;
#51641=FACE_OUTER_BOUND ( 'NONE', #5207, .T. ) ;
#51816=PRODUCT ( '13. Bolt M6x45', '13. Bolt M6x45', '', ( #6498 ) ) ;
#51985=B_SPLINE_CURVE_WITH_KNOTS ( 'NONE', 3,
 ( #42341, #62675, #36712, #63397, #4988, #25405 ),
 .UNSPECIFIED., .F., .F.,
 ( 4, 2, 4 ),
 ( 0.004189585287972434971, 0.006269578072783811573, 0.008349570857595188175 ),
 .UNSPECIFIED. ) ;
#52102=EDGE_LOOP ( 'NONE', ( #13463, #23492, #22269, #64146, #64948 ) ) ;
#52107=CARTESIAN_POINT ( 'NONE',  ( -4.358330484967983587, -6.451150163859152187, 0.7660251680141582087 ) ) ;
#52121=VERTEX_POINT ( 'NONE', #6501 ) ;
#52228=DIRECTION ( 'NONE',  ( -1.000000000000000000, 0.000000000000000000, 0.000000000000000000 ) ) ;
#52279=ORIENTED_EDGE ( 'NONE', *, *, #28091, .T. ) ;
#52357=VERTEX_POINT ( 'NONE', #63110 ) ;
#52406=EDGE_LOOP ( 'NONE', ( #32135, #44061, #48848, #60337, #38374 ) ) ;
#52436=EDGE_LOOP ( 'NONE', ( #31723, #9933, #11101 ) ) ;
#52510=CARTESIAN_POINT ( 'NONE',  ( 5.356721384544675502, 4.721886399977926807, 0.1324414877861175011 ) ) ;
#52542=ORIENTED_EDGE ( 'NONE', *, *, #44406, .T. ) ;
#52544=DIRECTION ( 'NONE',  ( 0.000000000000000000, 0.000000000000000000, 1.000000000000000000 ) ) ;
#52609=CARTESIAN_POINT ( 'NONE',  ( -4.041451884327381450, -7.000000000000002665, 1.082903768654759791 ) ) ;
#52661=VECTOR ( 'NONE', #53730, 1000.000000000000000 ) ;
#52829=( NAMED_UNIT ( * ) PLANE_ANGLE_UNIT ( ) SI_UNIT ( $, .RADIAN. ) );
#52871=DIRECTION ( 'NONE',  ( 0.000000000000000000, 0.000000000000000000, 1.000000000000000000 ) ) ;
#52882=DIRECTION ( 'NONE',  ( 1.000000000000000000, 0.000000000000000000, 0.000000000000000000 ) ) ;
#52927=AXIS2_PLACEMENT_3D ( 'NONE', #10271, #21498, #64416 ) ;
#53047=EDGE_LOOP ( 'NONE', ( #21121, #42150 ) ) ;
#53132=CARTESIAN_POINT ( 'NONE',  ( -5.705565085145812176, -4.117671386636407860, 0.02778322089669425093 ) ) ;
#53152=EDGE_CURVE ( 'NONE', #32986, #24001, #56878, .T. ) ;
#53162=EDGE_CURVE ( 'NONE', #22486, #23656, #58616, .T. ) ;
#53174=CARTESIAN_POINT ( 'NONE',  ( -0.7098155475105580869, 7.000000000000003553, 0.02753250691854559548 ) ) ;
#53424=CARTESIAN_POINT ( 'NONE',  ( 7.766025168014160762, -0.5488498361408512549, 0.7660251680141582087 ) ) ;
#53653=LINE ( 'NONE', #1159, #69579 ) ;
#53730=DIRECTION ( 'NONE',  ( -0.000000000000000000, -0.000000000000000000, -1.000000000000000000 ) ) ;
#53739=CARTESIAN_POINT ( 'NONE',  ( 6.767634268437467959, -2.278113600022081631, 0.1324414877861178896 ) ) ;
#53790=DIRECTION ( 'NONE',  ( 1.000000000000000000, 0.000000000000000000, 0.000000000000000000 ) ) ;
#53827=DIRECTION ( 'NONE',  ( 0.000000000000000000, 0.000000000000000000, 1.000000000000000000 ) ) ;
#53868=CIRCLE ( 'NONE', #29144, 5.000000000000000000 ) ;
#53965=VERTEX_POINT ( 'NONE', #13965 ) ;
#54024=CARTESIAN_POINT ( 'NONE',  ( 3.409623619629276625, -7.000000000000002665, 0.7804846576204699238 ) ) ;
#54071=CIRCLE ( 'NONE', #61905, 7.000000000000001776 ) ;
#54117=AXIS2_PLACEMENT_3D ( 'NONE', #20864, #52544, #52882 ) ;
#54183=CARTESIAN_POINT ( 'NONE',  ( -2.755190520427474699, 7.000000000000004441, 0.4949495880430779260 ) ) ;
#54189=EDGE_CURVE ( 'NONE', #22486, #56480, #48486, .T. ) ;
#54280=ORIENTED_EDGE ( 'NONE', *, *, #58702, .T. ) ;
#54302=ORIENTED_EDGE ( 'NONE', *, *, #30980, .F. ) ;
#54485=CARTESIAN_POINT ( 'NONE',  ( 0.000000000000000000, 0.000000000000000000, 0.000000000000000000 ) ) ;
#54534=VECTOR ( 'NONE', #42165, 1000.000000000000227 ) ;
#54576=SURFACE_STYLE_FILL_AREA ( #60527 ) ;
#54683=CIRCLE ( 'NONE', #55834, 7.000000000000001776 ) ;
#54737=CARTESIAN_POINT ( 'NONE',  ( 4.041451884327379673, -7.000000000000002665, 7.500000000000000000 ) ) ;
#55079=FACE_OUTER_BOUND ( 'NONE', #13946, .T. ) ;
#55135=DIRECTION ( 'NONE',  ( 1.000000000000000000, 0.000000000000000000, -0.000000000000000000 ) ) ;
#55149=CARTESIAN_POINT ( 'NONE',  ( -8.082903768654762899, 3.516382302766490365E-15, 7.500000000000000000 ) ) ;
#55186=EDGE_CURVE ( 'NONE', #57001, #22068, #22430, .T. ) ;
#55232=ORIENTED_EDGE ( 'NONE', *, *, #34759, .T. ) ;
#55234=ORIENTED_EDGE ( 'NONE', *, *, #38491, .T. ) ;
#55523=DIRECTION ( 'NONE',  ( 0.000000000000000000, 0.000000000000000000, -1.000000000000000000 ) ) ;
#55558=DIRECTION ( 'NONE',  ( 0.7071067811865426878, 8.659560562354873694E-17, -0.7071067811865524577 ) ) ;
#55726=ADVANCED_FACE ( 'NONE', ( #55079 ), #57691, .T. ) ;
#55827=EDGE_CURVE ( 'NONE', #52121, #7949, #56572, .T. ) ;
#55834=AXIS2_PLACEMENT_3D ( 'NONE', #12506, #16793, #27637 ) ;
#55893=CARTESIAN_POINT ( 'NONE',  ( 0.000000000000000000, 0.000000000000000000, 1.000000000000000000 ) ) ;
#55983=CARTESIAN_POINT ( 'NONE',  ( 4.041451884327376121, 7.000000000000007105, 1.082903768654759569 ) ) ;
#56142=CARTESIAN_POINT ( 'NONE',  ( -4.750000000000000000, 0.000000000000000000, 1.000000000000000000 ) ) ;
#56169=AXIS2_PLACEMENT_3D ( 'NONE', #28811, #45051, #22872 ) ;
#56259=DIRECTION ( 'NONE',  ( 1.000000000000000000, 0.000000000000000000, 0.000000000000000000 ) ) ;
#56292=CYLINDRICAL_SURFACE ( 'NONE', #48079, 5.000000000000000000 ) ;
#56409=DIRECTION ( 'NONE',  ( 1.000000000000000000, 1.073081856240828566E-16, 0.000000000000000000 ) ) ;
#56418=STYLED_ITEM ( 'NONE', ( #18494 ), #22466 ) ;
#56437=PRODUCT_DEFINITION_CONTEXT ( 'detailed design', #50483, 'design' ) ;
#56480=VERTEX_POINT ( 'NONE', #63030 ) ;
#56502=ORIENTED_EDGE ( 'NONE', *, *, #43481, .F. ) ;
#56542=FACE_OUTER_BOUND ( 'NONE', #52406, .T. ) ;
#56572=CIRCLE ( 'NONE', #42027, 0.2500000000000002220 ) ;
#56878=B_SPLINE_CURVE_WITH_KNOTS ( 'NONE', 3,
 ( #30045, #8952, #13877, #45232, #25124, #66659 ),
 .UNSPECIFIED., .F., .F.,
 ( 4, 2, 4 ),
 ( 0.004189585287972442777, 0.006269578072783818512, 0.008349570857595195114 ),
 .UNSPECIFIED. ) ;
#56935=DIRECTION ( 'NONE',  ( -0.000000000000000000, -0.000000000000000000, -1.000000000000000000 ) ) ;
#56995=CARTESIAN_POINT ( 'NONE',  ( 0.000000000000000000, 0.000000000000000000, 1.000000000000000000 ) ) ;
#57001=VERTEX_POINT ( 'NONE', #46841 ) ;
#57029=CARTESIAN_POINT ( 'NONE',  ( -4.041451884327381450, 7.000000000000006217, 1.082903768654761345 ) ) ;
#57167=ADVANCED_BREP_SHAPE_REPRESENTATION ( '', ( #3590, #42840 ), #2196 ) ;
#57207=UNCERTAINTY_MEASURE_WITH_UNIT (LENGTH_MEASURE( 1.000000000000000082E-05 ), #30997, 'distance_accuracy_value', 'NONE');
#57348=CARTESIAN_POINT ( 'NONE',  ( -6.418790567836333949, 2.882328613363593917, 0.02778322089669647138 ) ) ;
#57691=CONICAL_SURFACE ( 'NONE', #20627, 7.000000000000000888, 0.7853981633974500554 ) ;
#57749=( NAMED_UNIT ( * ) PLANE_ANGLE_UNIT ( ) SI_UNIT ( $, .RADIAN. ) );
#57982=SURFACE_SIDE_STYLE ('',( #41131 ) ) ;
#58103=PRESENTATION_STYLE_ASSIGNMENT (( #36324 ) ) ;
#58140=FACE_OUTER_BOUND ( 'NONE', #52436, .T. ) ;
#58418=LINE ( 'NONE', #68637, #18856 ) ;
#58616=B_SPLINE_CURVE_WITH_KNOTS ( 'NONE', 3,
 ( #19490, #40994, #62411, #8268, #35692, #7900, #29346, #46637 ),
 .UNSPECIFIED., .F., .F.,
 ( 4, 2, 2, 4 ),
 ( 0.008439684080927939078, 0.009486163742497470339, 0.01053264340406700160, 0.01262560272720606412 ),
 .UNSPECIFIED. ) ;
#58628=EDGE_CURVE ( 'NONE', #24120, #18515, #4189, .T. ) ;
#58702=EDGE_CURVE ( 'NONE', #38934, #53965, #29981, .T. ) ;
#58760=CONICAL_SURFACE ( 'NONE', #40808, 7.000000000000000888, 0.7853981633974500554 ) ;
#58829=EDGE_CURVE ( 'NONE', #18515, #57001, #40633, .T. ) ;
#59025=LINE ( 'NONE', #47482, #47326 ) ;
#59305=ADVANCED_FACE ( 'NONE', ( #3768 ), #43905, .F. ) ;
#59316=CIRCLE ( 'NONE', #2024, 7.000000000000001776 ) ;
#59484=AXIS2_PLACEMENT_3D ( 'NONE', #39218, #60617, #28611 ) ;
#59492=ADVANCED_FACE ( 'NONE', ( #26951 ), #61798, .T. ) ;
#59505=DIRECTION ( 'NONE',  ( 0.000000000000000000, 1.000000000000000000, 0.000000000000000000 ) ) ;
#59555=ORIENTED_EDGE ( 'NONE', *, *, #13164, .T. ) ;
#59642=EDGE_LOOP ( 'NONE', ( #29586, #18504, #48493 ) ) ;
#59668=CARTESIAN_POINT ( 'NONE',  ( 0.000000000000000000, 0.000000000000000000, 52.50000000000000000 ) ) ;
#59672=EDGE_LOOP ( 'NONE', ( #68969, #38184, #35626, #11725, #67653 ) ) ;
#59712=CARTESIAN_POINT ( 'NONE',  ( 6.938426666069066329, -1.982292489777644828, 0.2088670156639322040 ) ) ;
#59977=CARTESIAN_POINT ( 'NONE',  ( 0.000000000000000000, 0.000000000000000000, 0.000000000000000000 ) ) ;
#60171=CARTESIAN_POINT ( 'NONE',  ( 4.041451884327379673, -7.000000000000002665, 7.500000000000000000 ) ) ;
#60223=ORIENTED_EDGE ( 'NONE', *, *, #54189, .T. ) ;
#60273=UNCERTAINTY_MEASURE_WITH_UNIT (LENGTH_MEASURE( 1.000000000000000082E-05 ), #2943, 'distance_accuracy_value', 'NONE');
#60337=ORIENTED_EDGE ( 'NONE', *, *, #66986, .T. ) ;
#60428=DIRECTION ( 'NONE',  ( 0.8660254037844388186, 0.4999999999999998335, -0.000000000000000000 ) ) ;
#60440=B_SPLINE_CURVE_WITH_KNOTS ( 'NONE', 3,
 ( #34527, #65149, #7113, #22602, #28180, #28889, #65504, #55983 ),
 .UNSPECIFIED., .F., .F.,
 ( 4, 2, 2, 4 ),
 ( 0.01132179082380021552, 0.01341090848792873130, 0.01445546731999298833, 0.01550002615205724535 ),
 .UNSPECIFIED. ) ;
#60527=FILL_AREA_STYLE ('',( #33141 ) ) ;
#60617=DIRECTION ( 'NONE',  ( 0.8660254037844385966, -0.5000000000000001110, 0.000000000000000000 ) ) ;
#60679=SURFACE_STYLE_FILL_AREA ( #67028 ) ;
#60865=EDGE_CURVE ( 'NONE', #7949, #60935, #34006, .T. ) ;
#60935=VERTEX_POINT ( 'NONE', #16767 ) ;
#61000=DIRECTION ( 'NONE',  ( -0.000000000000000000, -0.000000000000000000, -1.000000000000000000 ) ) ;
#61129=AXIS2_PLACEMENT_3D ( 'NONE', #7864, #23703, #13140 ) ;
#61206=LINE ( 'NONE', #18656, #24082 ) ;
#61330=AXIS2_PLACEMENT_3D ( 'NONE', #12024, #59505, #32422 ) ;
#61345=LINE ( 'NONE', #18788, #12204 ) ;
#61378=( NAMED_UNIT ( * ) SI_UNIT ( $, .STERADIAN. ) SOLID_ANGLE_UNIT ( ) );
#61449=ORIENTED_EDGE ( 'NONE', *, *, #17869, .T. ) ;
#61497=LINE ( 'NONE', #24234, #52661 ) ;
#61511=CYLINDRICAL_SURFACE ( 'NONE', #48406, 3.000000000000000444 ) ;
#61558=CARTESIAN_POINT ( 'NONE',  ( -6.938426666069068993, 1.982292489777645272, 0.2088670156639333142 ) ) ;
#61746=AXIS2_PLACEMENT_3D ( 'NONE', #6325, #22520, #49259 ) ;
#61798=CONICAL_SURFACE ( 'NONE', #41635, 7.000000000000000888, 0.7853981633974500554 ) ;
#61818=DIRECTION ( 'NONE',  ( 0.000000000000000000, 0.000000000000000000, 1.000000000000000000 ) ) ;
#61829=ADVANCED_FACE ( 'NONE', ( #46020, #23480 ), #13265, .F. ) ;
#61905=AXIS2_PLACEMENT_3D ( 'NONE', #40408, #61818, #50264 ) ;
#61956=CARTESIAN_POINT ( 'NONE',  ( -7.000000000000000888, 0.000000000000000000, 0.000000000000000000 ) ) ;
#62058=EDGE_LOOP ( 'NONE', ( #51413, #14739, #49737, #67309, #51308, #16184, #33062 ) ) ;
#62161=DIRECTION ( 'NONE',  ( 0.5000000000000003331, -0.8660254037844383745, 0.000000000000000000 ) ) ;
#62376=DIRECTION ( 'NONE',  ( -0.000000000000000000, -0.000000000000000000, 1.000000000000000000 ) ) ;
#62411=CARTESIAN_POINT ( 'NONE',  ( -0.7098155475105565326, -7.000000000000003553, 0.02753250691854188317 ) ) ;
#62611=ORIENTED_EDGE ( 'NONE', *, *, #55827, .F. ) ;
#62675=CARTESIAN_POINT ( 'NONE',  ( -5.710692600061829438, 4.108790270285304302, 3.163668057994810583E-15 ) ) ;
#62884=ADVANCED_FACE ( 'NONE', ( #33315 ), #11498, .F. ) ;
#62988=DIRECTION ( 'NONE',  ( -0.000000000000000000, -0.000000000000000000, -1.000000000000000000 ) ) ;
#62999=CARTESIAN_POINT ( 'NONE',  ( 8.082903768654762899, -1.105959442090949618E-15, 7.500000000000000000 ) ) ;
#63030=CARTESIAN_POINT ( 'NONE',  ( 6.062177826491071286, -3.500000000000002220, 0.000000000000000000 ) ) ;
#63035=CYLINDRICAL_SURFACE ( 'NONE', #47723, 3.000000000000000444 ) ;
#63110=CARTESIAN_POINT ( 'NONE',  ( -7.511572993685801073E-16, 7.000000000000000888, 0.000000000000000000 ) ) ;
#63126=CARTESIAN_POINT ( 'NONE',  ( 0.000000000000000000, 0.000000000000000000, 7.500000000000000000 ) ) ;
#63161=CARTESIAN_POINT ( 'NONE',  ( -4.041451884327381450, -7.000000000000002665, 7.500000000000000000 ) ) ;
#63208=CARTESIAN_POINT ( 'NONE',  ( 0.7098900097155632638, -7.000000000000000888, -2.373649839567916678E-14 ) ) ;
#63346=ORIENTED_EDGE ( 'NONE', *, *, #20920, .T. ) ;
#63350=DIRECTION ( 'NONE',  ( 0.000000000000000000, 0.000000000000000000, 1.000000000000000000 ) ) ;
#63385=CARTESIAN_POINT ( 'NONE',  ( 4.682380833558962507, 5.889878495889167453, 0.4967607073414696539 ) ) ;
#63397=CARTESIAN_POINT ( 'NONE',  ( -4.683753779217435742, 5.887500484252664812, 0.4948905776603345075 ) ) ;
#63544=CARTESIAN_POINT ( 'NONE',  ( 0.000000000000000000, 0.000000000000000000, 0.7500000000000000000 ) ) ;
#63622=PRODUCT_DEFINITION_SHAPE ( 'NONE', 'NONE',  #6411 ) ;
#63678=AXIS2_PLACEMENT_3D ( 'NONE', #49840, #21706, #1581 ) ;
#63679=CARTESIAN_POINT ( 'NONE',  ( -4.750000000000000000, 0.000000000000000000, 0.7500000000000000000 ) ) ;
#63705=CARTESIAN_POINT ( 'NONE',  ( -1.403516486455610890, 7.000000000000006217, 0.1310752030855656391 ) ) ;
#63903=CARTESIAN_POINT ( 'NONE',  ( 0.000000000000000000, 0.000000000000000000, 0.2499999999999941436 ) ) ;
#64146=ORIENTED_EDGE ( 'NONE', *, *, #40528, .T. ) ;
#64416=DIRECTION ( 'NONE',  ( -1.000000000000000000, 0.000000000000000000, 0.000000000000000000 ) ) ;
#64548=ORIENTED_EDGE ( 'NONE', *, *, #12454, .F. ) ;
#64592=EDGE_CURVE ( 'NONE', #21751, #28960, #16554, .T. ) ;
#64910=DIRECTION ( 'NONE',  ( -1.000000000000000000, 0.000000000000000000, 0.000000000000000000 ) ) ;
#64943=ADVANCED_FACE ( 'NONE', ( #16475 ), #27651, .T. ) ;
#64948=ORIENTED_EDGE ( 'NONE', *, *, #58829, .F. ) ;
#65074=CARTESIAN_POINT ( 'NONE',  ( -7.511572993685801073E-16, 7.000000000000000888, 0.000000000000000000 ) ) ;
#65121=SURFACE_STYLE_USAGE ( .BOTH. , #27127 ) ;
#65149=CARTESIAN_POINT ( 'NONE',  ( 0.7098900097155618205, 7.000000000000007105, -1.987393404142764886E-14 ) ) ;
#65175=COLOUR_RGB ( '', 0.40784314, 0.44705882, 0.49803922) ;
#65183=EDGE_CURVE ( 'NONE', #17330, #23656, #31825, .T. ) ;
#65504=CARTESIAN_POINT ( 'NONE',  ( 3.728548500389067488, 7.000000000000006217, 0.9264520766856050304 ) ) ;
#65521=EDGE_CURVE ( 'NONE', #26743, #60935, #16565, .T. ) ;
#65541=CARTESIAN_POINT ( 'NONE',  ( -3.000000000000000444, 0.000000000000000000, 52.50000000000000000 ) ) ;
#65580=VECTOR ( 'NONE', #17515, 1000.000000000000000 ) ;
#65669=LINE ( 'NONE', #66355, #65580 ) ;
#65855=AXIS2_PLACEMENT_3D ( 'NONE', #44334, #55523, #7347 ) ;
#65919=PLANE ( 'NONE',  #59484 ) ;
#66095=ORIENTED_EDGE ( 'NONE', *, *, #43481, .T. ) ;
#66267=CARTESIAN_POINT ( 'NONE',  ( 4.041451884327376121, 7.000000000000007105, 7.500000000000000000 ) ) ;
#66304=DIRECTION ( 'NONE',  ( 1.000000000000000000, 0.000000000000000000, 0.000000000000000000 ) ) ;
#66314=SURFACE_STYLE_USAGE ( .BOTH. , #66678 ) ;
#66355=CARTESIAN_POINT ( 'NONE',  ( -4.041451884327381450, 7.000000000000006217, 7.500000000000000000 ) ) ;
#66659=CARTESIAN_POINT ( 'NONE',  ( 8.082903768654762899, -1.269775441351268174E-15, 1.082903768654759125 ) ) ;
#66678=SURFACE_SIDE_STYLE ('',( #60679 ) ) ;
#66696=CARTESIAN_POINT ( 'NONE',  ( -7.766391886667110001, -0.5482146608018571010, 0.7663918866669822139 ) ) ;
#66929=ORIENTED_EDGE ( 'NONE', *, *, #53162, .T. ) ;
#66986=EDGE_CURVE ( 'NONE', #28960, #24001, #58418, .T. ) ;
#67028=FILL_AREA_STYLE ('',( #13539 ) ) ;
#67108=PLANE ( 'NONE',  #48583 ) ;
#67184=ORIENTED_EDGE ( 'NONE', *, *, #40528, .F. ) ;
#67243=LINE ( 'NONE', #61956, #44330 ) ;
#67294=ORIENTED_EDGE ( 'NONE', *, *, #29463, .F. ) ;
#67309=ORIENTED_EDGE ( 'NONE', *, *, #17869, .F. ) ;
#67332=DIRECTION ( 'NONE',  ( 0.000000000000000000, 0.000000000000000000, 1.000000000000000000 ) ) ;
#67369=CIRCLE ( 'NONE', #8983, 3.000000000000000444 ) ;
#67498=EDGE_CURVE ( 'NONE', #25042, #8229, #24449, .T. ) ;
#67500=EDGE_CURVE ( 'NONE', #49555, #583, #37981, .T. ) ;
#67517=DIRECTION ( 'NONE',  ( 0.000000000000000000, 0.000000000000000000, 1.000000000000000000 ) ) ;
#67625=COLOUR_RGB ( '', 0.09019608, 0.27058824, 0.51372549) ;
#67653=ORIENTED_EDGE ( 'NONE', *, *, #53162, .F. ) ;
#67808=AXIS2_PLACEMENT_3D ( 'NONE', #40382, #44986, #55135 ) ;
#67840=( NAMED_UNIT ( * ) SI_UNIT ( $, .STERADIAN. ) SOLID_ANGLE_UNIT ( ) );
#67925=CARTESIAN_POINT ( 'NONE',  ( -6.767634268437469736, 2.278113600022081631, 0.1324414877861203599 ) ) ;
#68200=ORIENTED_EDGE ( 'NONE', *, *, #10289, .F. ) ;
#68527=( NAMED_UNIT ( * ) PLANE_ANGLE_UNIT ( ) SI_UNIT ( $, .RADIAN. ) );
#68637=CARTESIAN_POINT ( 'NONE',  ( 8.082903768654762899, -1.105959442090949618E-15, 7.500000000000000000 ) ) ;
#68890=DIRECTION ( 'NONE',  ( -0.5000000000000001110, -0.8660254037844385966, 0.000000000000000000 ) ) ;
#68969=ORIENTED_EDGE ( 'NONE', *, *, #34759, .F. ) ;
#69104=EDGE_CURVE ( 'NONE', #26743, #52121, #48316, .T. ) ;
#69278=ORIENTED_EDGE ( 'NONE', *, *, #18275, .T. ) ;
#69579=VECTOR ( 'NONE', #38575, 1000.000000000000000 ) ;
#69673=( NAMED_UNIT ( * ) SI_UNIT ( $, .STERADIAN. ) SOLID_ANGLE_UNIT ( ) );
ENDSEC;
END-ISO-10303-21;
